ISO-10303-21;
HEADER;
/* Generated by software containing ST-Developer
 * from STEP Tools, Inc. (www.steptools.com) 
 */

FILE_DESCRIPTION(
/* description */ ('Lifting hook block with sheave'),
/* implementation_level */ '2;1');

FILE_NAME(
/* name */ 'Flat Washer - M8.step',
/* time_stamp */ '2026-10-28T03:23:54-07:00',
/* author */ (''),
/* organization */ (''),
/* preprocessor_version */ 'ST-DEVELOPER v20.2',
/* originating_system */ 'Autodesk Translation Framework v15.17.0.0',
/* authorisation */ '');

FILE_SCHEMA (('AUTOMOTIVE_DESIGN { 1 0 10303 214 3 1 1 }'));
ENDSEC;

DATA;
#10=MECHANICAL_DESIGN_GEOMETRIC_PRESENTATION_REPRESENTATION('',(#364),#9391);
#304=SHAPE_REPRESENTATION_RELATIONSHIP('SRR','None',#9535,#334);
#334=ADVANCED_BREP_SHAPE_REPRESENTATION('',(#401),#9370);
#364=STYLED_ITEM('',(#9766),#401);
#401=MANIFOLD_SOLID_BREP('Body1',#4901);
#564=LINE('',#8127,#852);
#565=LINE('',#8133,#853);
#852=VECTOR('',#6579,0.42);
#853=VECTOR('',#6586,0.8);
#1051=CYLINDRICAL_SURFACE('',#5512,0.42);
#1052=CYLINDRICAL_SURFACE('',#5515,0.8);
#1161=FACE_BOUND('',#1684,.T.);
#1162=FACE_BOUND('',#1686,.T.);
#1338=FACE_OUTER_BOUND('',#1681,.T.);
#1339=FACE_OUTER_BOUND('',#1682,.T.);
#1340=FACE_OUTER_BOUND('',#1683,.T.);
#1341=FACE_OUTER_BOUND('',#1685,.T.);
#1681=EDGE_LOOP('',(#3752,#3753,#3754,#3755));
#1682=EDGE_LOOP('',(#3756,#3757,#3758,#3759));
#1683=EDGE_LOOP('',(#3760));
#1684=EDGE_LOOP('',(#3761));
#1685=EDGE_LOOP('',(#3762));
#1686=EDGE_LOOP('',(#3763));
#2036=CIRCLE('',#5513,0.42);
#2037=CIRCLE('',#5514,0.42);
#2038=CIRCLE('',#5516,0.8);
#2039=CIRCLE('',#5517,0.8);
#2381=VERTEX_POINT('',#8124);
#2382=VERTEX_POINT('',#8126);
#2383=VERTEX_POINT('',#8130);
#2384=VERTEX_POINT('',#8132);
#2880=EDGE_CURVE('',#2381,#2381,#2036,.T.);
#2881=EDGE_CURVE('',#2381,#2382,#564,.T.);
#2882=EDGE_CURVE('',#2382,#2382,#2037,.T.);
#2883=EDGE_CURVE('',#2383,#2383,#2038,.T.);
#2884=EDGE_CURVE('',#2383,#2384,#565,.T.);
#2885=EDGE_CURVE('',#2384,#2384,#2039,.T.);
#3752=ORIENTED_EDGE('',*,*,#2880,.F.);
#3753=ORIENTED_EDGE('',*,*,#2881,.T.);
#3754=ORIENTED_EDGE('',*,*,#2882,.T.);
#3755=ORIENTED_EDGE('',*,*,#2881,.F.);
#3756=ORIENTED_EDGE('',*,*,#2883,.F.);
#3757=ORIENTED_EDGE('',*,*,#2884,.T.);
#3758=ORIENTED_EDGE('',*,*,#2885,.T.);
#3759=ORIENTED_EDGE('',*,*,#2884,.F.);
#3760=ORIENTED_EDGE('',*,*,#2883,.T.);
#3761=ORIENTED_EDGE('',*,*,#2880,.T.);
#3762=ORIENTED_EDGE('',*,*,#2885,.F.);
#3763=ORIENTED_EDGE('',*,*,#2882,.F.);
#4514=PLANE('',#5518);
#4515=PLANE('',#5519);
#4714=ADVANCED_FACE('',(#1338),#1051,.F.);
#4715=ADVANCED_FACE('',(#1339),#1052,.T.);
#4716=ADVANCED_FACE('',(#1340,#1161),#4514,.T.);
#4717=ADVANCED_FACE('',(#1341,#1162),#4515,.F.);
#4901=CLOSED_SHELL('',(#4714,#4715,#4716,#4717));
#5511=AXIS2_PLACEMENT_3D('',#8122,#6573,#6574);
#5512=AXIS2_PLACEMENT_3D('',#8123,#6575,#6576);
#5513=AXIS2_PLACEMENT_3D('',#8125,#6577,#6578);
#5514=AXIS2_PLACEMENT_3D('',#8128,#6580,#6581);
#5515=AXIS2_PLACEMENT_3D('',#8129,#6582,#6583);
#5516=AXIS2_PLACEMENT_3D('',#8131,#6584,#6585);
#5517=AXIS2_PLACEMENT_3D('',#8134,#6587,#6588);
#5518=AXIS2_PLACEMENT_3D('',#8135,#6589,#6590);
#5519=AXIS2_PLACEMENT_3D('',#8136,#6591,#6592);
#6573=DIRECTION('axis',(0.,0.,1.));
#6574=DIRECTION('refdir',(1.,0.,0.));
#6575=DIRECTION('center_axis',(0.,1.,0.));
#6576=DIRECTION('ref_axis',(1.,0.,0.));
#6577=DIRECTION('center_axis',(0.,-1.,0.));
#6578=DIRECTION('ref_axis',(1.,0.,0.));
#6579=DIRECTION('',(0.,-1.,0.));
#6580=DIRECTION('center_axis',(0.,-1.,0.));
#6581=DIRECTION('ref_axis',(1.,0.,0.));
#6582=DIRECTION('center_axis',(0.,1.,0.));
#6583=DIRECTION('ref_axis',(1.,0.,0.));
#6584=DIRECTION('center_axis',(0.,1.,0.));
#6585=DIRECTION('ref_axis',(1.,0.,0.));
#6586=DIRECTION('',(0.,-1.,0.));
#6587=DIRECTION('center_axis',(0.,1.,0.));
#6588=DIRECTION('ref_axis',(1.,0.,0.));
#6589=DIRECTION('center_axis',(0.,1.,0.));
#6590=DIRECTION('ref_axis',(1.,0.,0.));
#6591=DIRECTION('center_axis',(0.,1.,0.));
#6592=DIRECTION('ref_axis',(1.,0.,0.));
#8122=CARTESIAN_POINT('',(0.,0.,0.));
#8123=CARTESIAN_POINT('Origin',(0.,0.,0.));
#8124=CARTESIAN_POINT('',(-0.42,0.16,5.14351655641888E-17));
#8125=CARTESIAN_POINT('Origin',(0.,0.16,0.));
#8126=CARTESIAN_POINT('',(-0.42,0.,5.14351655641888E-17));
#8127=CARTESIAN_POINT('',(-0.42,0.,5.14351655641888E-17));
#8128=CARTESIAN_POINT('Origin',(0.,0.,0.));
#8129=CARTESIAN_POINT('Origin',(0.,0.,0.));
#8130=CARTESIAN_POINT('',(-0.8,0.16,9.79717439317883E-17));
#8131=CARTESIAN_POINT('Origin',(0.,0.16,0.));
#8132=CARTESIAN_POINT('',(-0.8,0.,9.79717439317883E-17));
#8133=CARTESIAN_POINT('',(-0.8,0.,9.79717439317883E-17));
#8134=CARTESIAN_POINT('Origin',(0.,0.,0.));
#8135=CARTESIAN_POINT('Origin',(0.,0.16,0.));
#8136=CARTESIAN_POINT('Origin',(0.,0.,0.));
#9333=UNCERTAINTY_MEASURE_WITH_UNIT(LENGTH_MEASURE(0.001),#9392,
'DISTANCE_ACCURACY_VALUE',
'Maximum model space distance between geometric entities at asserted c
onnectivities');
#9354=UNCERTAINTY_MEASURE_WITH_UNIT(LENGTH_MEASURE(0.001),#9392,
'DISTANCE_ACCURACY_VALUE',
'Maximum model space distance between geometric entities at asserted c
onnectivities');
#9370=(
GEOMETRIC_REPRESENTATION_CONTEXT(3)
GLOBAL_UNCERTAINTY_ASSIGNED_CONTEXT((#9333))
GLOBAL_UNIT_ASSIGNED_CONTEXT((#9392,#9394,#9395))
REPRESENTATION_CONTEXT('','3D')
);
#9391=(
GEOMETRIC_REPRESENTATION_CONTEXT(3)
GLOBAL_UNCERTAINTY_ASSIGNED_CONTEXT((#9354))
GLOBAL_UNIT_ASSIGNED_CONTEXT((#9392,#9394,#9395))
REPRESENTATION_CONTEXT('','3D')
);
#9392=(
LENGTH_UNIT()
NAMED_UNIT(*)
SI_UNIT(.CENTI.,.METRE.)
);
#9394=(
NAMED_UNIT(*)
PLANE_ANGLE_UNIT()
SI_UNIT($,.RADIAN.)
);
#9395=(
NAMED_UNIT(*)
SI_UNIT($,.STERADIAN.)
SOLID_ANGLE_UNIT()
);
#9411=SHAPE_DEFINITION_REPRESENTATION(#9447,#9535);
#9447=PRODUCT_DEFINITION_SHAPE('',$,#9572);
#9535=SHAPE_REPRESENTATION('',(#5511),#9370);
#9556=PRODUCT_DEFINITION_CONTEXT('part definition',#9666,'design');
#9572=PRODUCT_DEFINITION('Flat Washer - M8','Flat Washer - M8',#9608,#9556);
#9608=PRODUCT_DEFINITION_FORMATION('',$,#9683);
#9666=APPLICATION_CONTEXT(
'Core Data for Automotive Mechanical Design Process');
#9667=PRODUCT_CONTEXT('part definition',#9666,'mechanical');
#9683=PRODUCT('Flat Washer - M8','Flat Washer - M8','Flat Washer - M8',
(#9667));
#9760=COLOUR_RGB('Black',0.12,0.14,0.17);
#9761=FILL_AREA_STYLE_COLOUR('',#9760);
#9762=FILL_AREA_STYLE('',(#9761));
#9763=SURFACE_STYLE_FILL_AREA(#9762);
#9764=SURFACE_SIDE_STYLE('',(#9763));
#9765=SURFACE_STYLE_USAGE(.BOTH.,#9764);
#9766=PRESENTATION_STYLE_ASSIGNMENT((#9765));
ENDSEC;
END-ISO-10303-21;
